ISO-10303-21;
HEADER;
FILE_DESCRIPTION((''),'2;1');
FILE_NAME('DIN 6799 - 3.2 Retaining Washer (E-Clip).step','2026-10-06T07:37:42+05:00',(''),(''),'','','');
FILE_SCHEMA (('AUTOMOTIVE_DESIGN { 1 0 10303 214 3 1 1 }'));
ENDSEC;
DATA;
#10=MECHANICAL_DESIGN_GEOMETRIC_PRESENTATION_REPRESENTATION('',(#384),#18757);
#350=SHAPE_REPRESENTATION_RELATIONSHIP('SRR','None',#18868,#367) ;
#367=ADVANCED_BREP_SHAPE_REPRESENTATION('',(#401),#18751) ;
#384=STYLED_ITEM('',(#18962),#401) ;
#401=MANIFOLD_SOLID_BREP('DIN 6799 - 3.2 Retaining Washer (E-Clip)',#9553) ;
#592=CYLINDRICAL_SURFACE('',#10246,1.59999999999999) ;
#593=CYLINDRICAL_SURFACE('',#10251,3.65) ;
#911=PLANE('',#10242) ;
#912=PLANE('',#10243) ;
#913=PLANE('',#10244) ;
#914=PLANE('',#10245) ;
#915=PLANE('',#10249) ;
#916=PLANE('',#10253) ;
#1356=FACE_OUTER_BOUND('',#1956,.T.) ;
#1357=FACE_OUTER_BOUND('',#1957,.T.) ;
#1358=FACE_OUTER_BOUND('',#1958,.T.) ;
#1359=FACE_OUTER_BOUND('',#1959,.T.) ;
#1360=FACE_OUTER_BOUND('',#1960,.T.) ;
#1361=FACE_OUTER_BOUND('',#1961,.T.) ;
#1362=FACE_OUTER_BOUND('',#1962,.T.) ;
#1363=FACE_OUTER_BOUND('',#1963,.T.) ;
#1956=EDGE_LOOP('',(#7669,#7670,#7671,#7672)) ;
#1957=EDGE_LOOP('',(#7673,#7674,#7675,#7676)) ;
#1958=EDGE_LOOP('',(#7677,#7678,#7679,#7680)) ;
#1959=EDGE_LOOP('',(#7681,#7682,#7683,#7684)) ;
#1960=EDGE_LOOP('',(#7685,#7686,#7687,#7688)) ;
#1961=EDGE_LOOP('',(#7689,#7690,#7691,#7692,#7693,#7694)) ;
#1962=EDGE_LOOP('',(#7695,#7696,#7697,#7698)) ;
#1963=EDGE_LOOP('',(#7699,#7700,#7701,#7702,#7703,#7704)) ;
#2652=LINE('',#15235,#3423) ;
#2653=LINE('',#15237,#3424) ;
#2654=LINE('',#15239,#3425) ;
#2655=LINE('',#15240,#3426) ;
#2656=LINE('',#15244,#3427) ;
#2657=LINE('',#15246,#3428) ;
#2658=LINE('',#15248,#3429) ;
#2659=LINE('',#15249,#3430) ;
#2660=LINE('',#15252,#3431) ;
#2661=LINE('',#15254,#3432) ;
#2662=LINE('',#15255,#3433) ;
#2663=LINE('',#15258,#3434) ;
#2664=LINE('',#15260,#3435) ;
#2665=LINE('',#15261,#3436) ;
#3423=VECTOR('',#12126,10.) ;
#3424=VECTOR('',#12127,10.) ;
#3425=VECTOR('',#12128,10.) ;
#3426=VECTOR('',#12129,10.) ;
#3427=VECTOR('',#12132,10.) ;
#3428=VECTOR('',#12133,10.) ;
#3429=VECTOR('',#12134,10.) ;
#3430=VECTOR('',#12135,10.) ;
#3431=VECTOR('',#12138,10.) ;
#3432=VECTOR('',#12139,10.) ;
#3433=VECTOR('',#12140,10.) ;
#3434=VECTOR('',#12143,10.) ;
#3435=VECTOR('',#12144,10.) ;
#3436=VECTOR('',#12145,10.) ;
#3988=CIRCLE('',#10247,1.59999999999999) ;
#3989=CIRCLE('',#10248,1.59999999999999) ;
#3990=CIRCLE('',#10250,3.65) ;
#3991=CIRCLE('',#10252,3.65) ;
#4585=VERTEX_POINT('',#15233) ;
#4586=VERTEX_POINT('',#15234) ;
#4587=VERTEX_POINT('',#15236) ;
#4588=VERTEX_POINT('',#15238) ;
#4589=VERTEX_POINT('',#15242) ;
#4590=VERTEX_POINT('',#15243) ;
#4591=VERTEX_POINT('',#15245) ;
#4592=VERTEX_POINT('',#15247) ;
#4593=VERTEX_POINT('',#15251) ;
#4594=VERTEX_POINT('',#15253) ;
#4595=VERTEX_POINT('',#15257) ;
#4596=VERTEX_POINT('',#15259) ;
#5681=EDGE_CURVE('',#4585,#4586,#2652,.T.) ;
#5682=EDGE_CURVE('',#4587,#4585,#2653,.T.) ;
#5683=EDGE_CURVE('',#4588,#4587,#2654,.T.) ;
#5684=EDGE_CURVE('',#4586,#4588,#2655,.T.) ;
#5685=EDGE_CURVE('',#4589,#4590,#2656,.T.) ;
#5686=EDGE_CURVE('',#4589,#4591,#2657,.T.) ;
#5687=EDGE_CURVE('',#4592,#4591,#2658,.T.) ;
#5688=EDGE_CURVE('',#4590,#4592,#2659,.T.) ;
#5689=EDGE_CURVE('',#4586,#4593,#2660,.T.) ;
#5690=EDGE_CURVE('',#4594,#4588,#2661,.T.) ;
#5691=EDGE_CURVE('',#4593,#4594,#2662,.T.) ;
#5692=EDGE_CURVE('',#4595,#4589,#2663,.T.) ;
#5693=EDGE_CURVE('',#4596,#4595,#2664,.T.) ;
#5694=EDGE_CURVE('',#4591,#4596,#2665,.T.) ;
#5695=EDGE_CURVE('',#4587,#4592,#3988,.T.) ;
#5696=EDGE_CURVE('',#4585,#4590,#3989,.T.) ;
#5697=EDGE_CURVE('',#4594,#4596,#3990,.T.) ;
#5698=EDGE_CURVE('',#4593,#4595,#3991,.T.) ;
#7669=ORIENTED_EDGE('',*,*,#5681,.F.) ;
#7670=ORIENTED_EDGE('',*,*,#5682,.F.) ;
#7671=ORIENTED_EDGE('',*,*,#5683,.F.) ;
#7672=ORIENTED_EDGE('',*,*,#5684,.F.) ;
#7673=ORIENTED_EDGE('',*,*,#5685,.F.) ;
#7674=ORIENTED_EDGE('',*,*,#5686,.T.) ;
#7675=ORIENTED_EDGE('',*,*,#5687,.F.) ;
#7676=ORIENTED_EDGE('',*,*,#5688,.F.) ;
#7677=ORIENTED_EDGE('',*,*,#5689,.F.) ;
#7678=ORIENTED_EDGE('',*,*,#5684,.T.) ;
#7679=ORIENTED_EDGE('',*,*,#5690,.F.) ;
#7680=ORIENTED_EDGE('',*,*,#5691,.F.) ;
#7681=ORIENTED_EDGE('',*,*,#5692,.F.) ;
#7682=ORIENTED_EDGE('',*,*,#5693,.F.) ;
#7683=ORIENTED_EDGE('',*,*,#5694,.F.) ;
#7684=ORIENTED_EDGE('',*,*,#5686,.F.) ;
#7685=ORIENTED_EDGE('',*,*,#5688,.T.) ;
#7686=ORIENTED_EDGE('',*,*,#5695,.F.) ;
#7687=ORIENTED_EDGE('',*,*,#5682,.T.) ;
#7688=ORIENTED_EDGE('',*,*,#5696,.T.) ;
#7689=ORIENTED_EDGE('',*,*,#5687,.T.) ;
#7690=ORIENTED_EDGE('',*,*,#5694,.T.) ;
#7691=ORIENTED_EDGE('',*,*,#5697,.F.) ;
#7692=ORIENTED_EDGE('',*,*,#5690,.T.) ;
#7693=ORIENTED_EDGE('',*,*,#5683,.T.) ;
#7694=ORIENTED_EDGE('',*,*,#5695,.T.) ;
#7695=ORIENTED_EDGE('',*,*,#5693,.T.) ;
#7696=ORIENTED_EDGE('',*,*,#5698,.F.) ;
#7697=ORIENTED_EDGE('',*,*,#5691,.T.) ;
#7698=ORIENTED_EDGE('',*,*,#5697,.T.) ;
#7699=ORIENTED_EDGE('',*,*,#5685,.T.) ;
#7700=ORIENTED_EDGE('',*,*,#5696,.F.) ;
#7701=ORIENTED_EDGE('',*,*,#5681,.T.) ;
#7702=ORIENTED_EDGE('',*,*,#5689,.T.) ;
#7703=ORIENTED_EDGE('',*,*,#5698,.T.) ;
#7704=ORIENTED_EDGE('',*,*,#5692,.T.) ;
#9292=ADVANCED_FACE('',(#1356),#911,.F.) ;
#9293=ADVANCED_FACE('',(#1357),#912,.F.) ;
#9294=ADVANCED_FACE('',(#1358),#913,.F.) ;
#9295=ADVANCED_FACE('',(#1359),#914,.F.) ;
#9296=ADVANCED_FACE('',(#1360),#592,.F.) ;
#9297=ADVANCED_FACE('',(#1361),#915,.T.) ;
#9298=ADVANCED_FACE('',(#1362),#593,.T.) ;
#9299=ADVANCED_FACE('',(#1363),#916,.T.) ;
#9553=CLOSED_SHELL('',(#9292,#9293,#9294,#9295,#9296,#9297,#9298,#9299)) ;
#10241=AXIS2_PLACEMENT_3D('',#15231,#12122,#12123) ;
#10242=AXIS2_PLACEMENT_3D('',#15232,#12124,#12125) ;
#10243=AXIS2_PLACEMENT_3D('',#15241,#12130,#12131) ;
#10244=AXIS2_PLACEMENT_3D('',#15250,#12136,#12137) ;
#10245=AXIS2_PLACEMENT_3D('',#15256,#12141,#12142) ;
#10246=AXIS2_PLACEMENT_3D('',#15262,#12146,#12147) ;
#10247=AXIS2_PLACEMENT_3D('',#15263,#12148,#12149) ;
#10248=AXIS2_PLACEMENT_3D('',#15264,#12150,#12151) ;
#10249=AXIS2_PLACEMENT_3D('',#15265,#12152,#12153) ;
#10250=AXIS2_PLACEMENT_3D('',#15266,#12154,#12155) ;
#10251=AXIS2_PLACEMENT_3D('',#15267,#12156,#12157) ;
#10252=AXIS2_PLACEMENT_3D('',#15268,#12158,#12159) ;
#10253=AXIS2_PLACEMENT_3D('',#15269,#12160,#12161) ;
#12122=DIRECTION('axis',(0.,0.,1.)) ;
#12123=DIRECTION('refdir',(1.,0.,0.)) ;
#12124=DIRECTION('center_axis',(0.,0.,1.)) ;
#12125=DIRECTION('ref_axis',(1.,0.,0.)) ;
#12126=DIRECTION('',(1.,0.,0.)) ;
#12127=DIRECTION('',(0.,-1.,0.)) ;
#12128=DIRECTION('',(-1.,0.,0.)) ;
#12129=DIRECTION('',(0.,1.,0.)) ;
#12130=DIRECTION('center_axis',(0.,0.,1.)) ;
#12131=DIRECTION('ref_axis',(1.,0.,0.)) ;
#12132=DIRECTION('',(1.,0.,0.)) ;
#12133=DIRECTION('',(0.,1.,0.)) ;
#12134=DIRECTION('',(-1.,0.,0.)) ;
#12135=DIRECTION('',(0.,1.,0.)) ;
#12136=DIRECTION('center_axis',(1.,0.,0.)) ;
#12137=DIRECTION('ref_axis',(0.,0.,-1.)) ;
#12138=DIRECTION('',(0.,0.,-1.)) ;
#12139=DIRECTION('',(0.,0.,1.)) ;
#12140=DIRECTION('',(0.,1.,0.)) ;
#12141=DIRECTION('center_axis',(-1.,0.,0.)) ;
#12142=DIRECTION('ref_axis',(0.,0.,1.)) ;
#12143=DIRECTION('',(0.,0.,1.)) ;
#12144=DIRECTION('',(0.,-1.,0.)) ;
#12145=DIRECTION('',(0.,0.,-1.)) ;
#12146=DIRECTION('center_axis',(0.,-1.,0.)) ;
#12147=DIRECTION('ref_axis',(-1.83697019872103E-16,0.,1.)) ;
#12148=DIRECTION('center_axis',(0.,-1.,0.)) ;
#12149=DIRECTION('ref_axis',(1.,0.,0.)) ;
#12150=DIRECTION('center_axis',(0.,-1.,0.)) ;
#12151=DIRECTION('ref_axis',(1.,0.,0.)) ;
#12152=DIRECTION('center_axis',(0.,1.,0.)) ;
#12153=DIRECTION('ref_axis',(0.,0.,1.)) ;
#12154=DIRECTION('center_axis',(0.,-1.,0.)) ;
#12155=DIRECTION('ref_axis',(1.,0.,0.)) ;
#12156=DIRECTION('center_axis',(0.,-1.,0.)) ;
#12157=DIRECTION('ref_axis',(-1.83697019872103E-16,0.,1.)) ;
#12158=DIRECTION('center_axis',(0.,-1.,0.)) ;
#12159=DIRECTION('ref_axis',(1.,0.,0.)) ;
#12160=DIRECTION('center_axis',(0.,-1.,0.)) ;
#12161=DIRECTION('ref_axis',(0.,0.,-1.)) ;
#15231=CARTESIAN_POINT('',(0.,0.,0.)) ;
#15232=CARTESIAN_POINT('Origin',(70.4,44.1,34.)) ;
#15233=CARTESIAN_POINT('',(73.2489995996797,44.2,34.)) ;
#15234=CARTESIAN_POINT('',(73.6,44.2,34.)) ;
#15235=CARTESIAN_POINT('',(72.,44.2,34.)) ;
#15236=CARTESIAN_POINT('',(73.2489995996797,44.8,34.)) ;
#15237=CARTESIAN_POINT('',(73.2489995996797,44.5,34.)) ;
#15238=CARTESIAN_POINT('',(73.6,44.8,34.)) ;
#15239=CARTESIAN_POINT('',(73.025,44.8,34.)) ;
#15240=CARTESIAN_POINT('',(73.6,44.1,34.)) ;
#15241=CARTESIAN_POINT('Origin',(70.4,44.1,34.)) ;
#15242=CARTESIAN_POINT('',(70.4,44.2,34.)) ;
#15243=CARTESIAN_POINT('',(70.7510004003203,44.2,34.)) ;
#15244=CARTESIAN_POINT('',(72.,44.2,34.)) ;
#15245=CARTESIAN_POINT('',(70.4,44.8,34.)) ;
#15246=CARTESIAN_POINT('',(70.4,44.1,34.)) ;
#15247=CARTESIAN_POINT('',(70.7510004003203,44.8,34.)) ;
#15248=CARTESIAN_POINT('',(73.025,44.8,34.)) ;
#15249=CARTESIAN_POINT('',(70.7510004003203,44.5,34.)) ;
#15250=CARTESIAN_POINT('Origin',(73.6,44.1,34.)) ;
#15251=CARTESIAN_POINT('',(73.6,44.2,31.7193750595351)) ;
#15252=CARTESIAN_POINT('',(73.6,44.2,34.5)) ;
#15253=CARTESIAN_POINT('',(73.6,44.8,31.7193750595351)) ;
#15254=CARTESIAN_POINT('',(73.6,44.8,34.5)) ;
#15255=CARTESIAN_POINT('',(73.6,44.5,31.7193750595351)) ;
#15256=CARTESIAN_POINT('Origin',(70.4,44.1,31.)) ;
#15257=CARTESIAN_POINT('',(70.4,44.2,31.7193750595351)) ;
#15258=CARTESIAN_POINT('',(70.4,44.2,33.)) ;
#15259=CARTESIAN_POINT('',(70.4,44.8,31.7193750595351)) ;
#15260=CARTESIAN_POINT('',(70.4,44.5,31.7193750595351)) ;
#15261=CARTESIAN_POINT('',(70.4,44.8,33.)) ;
#15262=CARTESIAN_POINT('Origin',(72.,44.5,35.)) ;
#15263=CARTESIAN_POINT('Origin',(72.,44.8,35.)) ;
#15264=CARTESIAN_POINT('Origin',(72.,44.2,35.)) ;
#15265=CARTESIAN_POINT('Origin',(75.65,44.8,35.)) ;
#15266=CARTESIAN_POINT('Origin',(72.,44.8,35.)) ;
#15267=CARTESIAN_POINT('Origin',(72.,44.5,35.)) ;
#15268=CARTESIAN_POINT('Origin',(72.,44.2,35.)) ;
#15269=CARTESIAN_POINT('Origin',(73.6,44.2,35.)) ;
#18732=UNCERTAINTY_MEASURE_WITH_UNIT(LENGTH_MEASURE(0.01),#18758,
'DISTANCE_ACCURACY_VALUE',
'Maximum model space distance between geometric entities at asserted c
onnectivities') ;
#18738=UNCERTAINTY_MEASURE_WITH_UNIT(LENGTH_MEASURE(0.01),#18758,
'DISTANCE_ACCURACY_VALUE',
'Maximum model space distance between geometric entities at asserted c
onnectivities') ;
#18751=(
GEOMETRIC_REPRESENTATION_CONTEXT(3)
GLOBAL_UNCERTAINTY_ASSIGNED_CONTEXT((#18732))
GLOBAL_UNIT_ASSIGNED_CONTEXT((#18758,#18760,#18761))
REPRESENTATION_CONTEXT('','3D')
) ;
#18757=(
GEOMETRIC_REPRESENTATION_CONTEXT(3)
GLOBAL_UNCERTAINTY_ASSIGNED_CONTEXT((#18738))
GLOBAL_UNIT_ASSIGNED_CONTEXT((#18758,#18760,#18761))
REPRESENTATION_CONTEXT('','3D')
) ;
#18758=(
LENGTH_UNIT()
NAMED_UNIT(*)
SI_UNIT(.MILLI.,.METRE.)
) ;
#18760=(
NAMED_UNIT(*)
PLANE_ANGLE_UNIT()
SI_UNIT($,.RADIAN.)
) ;
#18761=(
NAMED_UNIT(*)
SI_UNIT($,.STERADIAN.)
SOLID_ANGLE_UNIT()
) ;
#18774=SHAPE_DEFINITION_REPRESENTATION(#18792,#18868) ;
#18792=PRODUCT_DEFINITION_SHAPE('',$,#18887) ;
#18868=SHAPE_REPRESENTATION('',(#10241),#18751) ;
#18874=PRODUCT_DEFINITION_CONTEXT('part definition',#18930,'design') ;
#18887=PRODUCT_DEFINITION('DIN 6799 - 3.2 Retaining Washer (E-Clip)',
'DIN 6799 - 3.2 Retaining Washer (E-Clip)',#18905,#18874) ;
#18905=PRODUCT_DEFINITION_FORMATION('',$,#18944) ;
#18930=APPLICATION_CONTEXT(
'Core Data for Automotive Mechanical Design Process') ;
#18931=PRODUCT_CONTEXT('part definition',#18930,'mechanical') ;
#18944=PRODUCT('DIN 6799 - 3.2 Retaining Washer (E-Clip)',
'DIN 6799 - 3.2 Retaining Washer (E-Clip)',$,(#18931)) ;
#18962=PRESENTATION_STYLE_ASSIGNMENT((#18980)) ;
#18980=SURFACE_STYLE_USAGE(.BOTH.,#18998) ;
#18998=SURFACE_SIDE_STYLE('',(#19016)) ;
#19016=SURFACE_STYLE_FILL_AREA(#19034) ;
#19034=FILL_AREA_STYLE(
'MAS-253 Metallic Sheet - DIN 6799 - 3.2 Retaining Washer (E-Clip)',(#19052)) ;
#19052=FILL_AREA_STYLE_COLOUR(
'MAS-253 Metallic Sheet - DIN 6799 - 3.2 Retaining Washer (E-Clip)',#19070) ;
#19070=COLOUR_RGB(
'MAS-253 Metallic Sheet - DIN 6799 - 3.2 Retaining Washer (E-Clip)', 0.09019608, 0.27058824, 0.51372549) ;
ENDSEC;
END-ISO-10303-21;
